ISO-10303-21;
HEADER;
FILE_DESCRIPTION (('STEP AP214'),
    '1' );
FILE_NAME ('angular contact ball bearing_68_iso_ISO 15 ABB - 1710 - 20,SI,NC,20_68.step',
    '2026-10-27T17:01:19',
    ( '' ),
    ( '' ),
    'SwSTEP 2.0',
    'SolidWorks 2026',
    '' );
FILE_SCHEMA (( 'AUTOMOTIVE_DESIGN' ));
ENDSEC;

DATA;
#16=ORIENTED_EDGE ( 'NONE', *, *, #2742, .F. ) ;
#25=EDGE_CURVE ( 'NONE', #3163, #4002, #6451, .T. ) ;
#31=EDGE_CURVE ( 'NONE', #4518, #4002, #1965, .T. ) ;
#39=DIRECTION ( 'NONE',  ( 1.000000000000000000, 0.000000000000000000, 0.000000000000000000 ) ) ;
#56=CARTESIAN_POINT ( 'NONE',  ( -20.63749999999999574, 0.000000000000000000, -6.975000000000000533 ) ) ;
#62=EDGE_LOOP ( 'NONE', ( #9424, #13653, #13087, #10601 ) ) ;
#148=FACE_BOUND ( 'NONE', #8389, .T. ) ;
#169=CARTESIAN_POINT ( 'NONE',  ( 1.500000000000001332, 0.000000000000000000, 0.000000000000000000 ) ) ;
#189=AXIS2_PLACEMENT_3D ( 'NONE', #8607, #13111, #14291 ) ;
#200=VECTOR ( 'NONE', #9426, 1000.000000000000000 ) ;
#201=CARTESIAN_POINT ( 'NONE',  ( 0.000000000000000000, 0.000000000000000000, 6.250000000000000000 ) ) ;
#222=EDGE_CURVE ( 'NONE', #5688, #13812, #7865, .T. ) ;
#223=CIRCLE ( 'NONE', #9439, 5.000000000000000000 ) ;
#227=DIRECTION ( 'NONE',  ( 0.000000000000000000, 0.000000000000000000, -1.000000000000000000 ) ) ;
#253=ORIENTED_EDGE ( 'NONE', *, *, #3737, .F. ) ;
#270=PRODUCT_DEFINITION_FORMATION_WITH_SPECIFIED_SOURCE ( 'ANY', '', #8554, .NOT_KNOWN. ) ;
#294=FACE_OUTER_BOUND ( 'NONE', #6811, .T. ) ;
#301=FACE_OUTER_BOUND ( 'NONE', #4804, .T. ) ;
#305=DIRECTION ( 'NONE',  ( 1.000000000000000000, 0.000000000000000000, 0.000000000000000000 ) ) ;
#330=CARTESIAN_POINT ( 'NONE',  ( -20.63749999999999574, 0.000000000000000000, 0.000000000000000000 ) ) ;
#370=CARTESIAN_POINT ( 'NONE',  ( -1.400000000000001910, 0.000000000000000000, 0.000000000000000000 ) ) ;
#389=DIRECTION ( 'NONE',  ( 1.000000000000000000, 0.000000000000000000, 0.000000000000000000 ) ) ;
#402=DIRECTION ( 'NONE',  ( 1.000000000000000000, 0.000000000000000000, 0.000000000000000000 ) ) ;
#407=EDGE_CURVE ( 'NONE', #12943, #442, #6308, .T. ) ;
#442=VERTEX_POINT ( 'NONE', #4964 ) ;
#452=DIRECTION ( 'NONE',  ( 0.000000000000000000, 0.000000000000000000, -1.000000000000000000 ) ) ;
#453=CARTESIAN_POINT ( 'NONE',  ( -0.5590169943749470072, 0.000000000000000000, -5.750000000000000000 ) ) ;
#505=EDGE_LOOP ( 'NONE', ( #10225, #3201, #8699, #7735 ) ) ;
#516=DIRECTION ( 'NONE',  ( 0.000000000000000000, 0.000000000000000000, -1.000000000000000000 ) ) ;
#524=ORIENTED_EDGE ( 'NONE', *, *, #2629, .F. ) ;
#530=DIRECTION ( 'NONE',  ( 1.000000000000000000, 0.000000000000000000, 0.000000000000000000 ) ) ;
#630=DIRECTION ( 'NONE',  ( -0.000000000000000000, 0.000000000000000000, 1.000000000000000000 ) ) ;
#638=DIRECTION ( 'NONE',  ( 0.000000000000000000, 0.000000000000000000, -1.000000000000000000 ) ) ;
#640=ORIENTED_EDGE ( 'NONE', *, *, #6281, .F. ) ;
#648=FACE_OUTER_BOUND ( 'NONE', #11384, .T. ) ;
#660=DIRECTION ( 'NONE',  ( 0.000000000000000000, 0.000000000000000000, -1.000000000000000000 ) ) ;
#686=TOROIDAL_SURFACE ( 'NONE', #1163, 5.100000000000000533, 0.1000000000000001582 ) ;
#689=VERTEX_POINT ( 'NONE', #9677 ) ;
#690=LINE ( 'NONE', #5287, #12287 ) ;
#697=AXIS2_PLACEMENT_3D ( 'NONE', #6901, #1132, #14574 ) ;
#721=CIRCLE ( 'NONE', #12751, 0.1000000000000002554 ) ;
#732=UNCERTAINTY_MEASURE_WITH_UNIT (LENGTH_MEASURE( 1.000000000000000082E-05 ), #9644, 'distance_accuracy_value', 'NONE');
#741=AXIS2_PLACEMENT_3D ( 'NONE', #2991, #7488, #11983 ) ;
#753=DIRECTION ( 'NONE',  ( 0.000000000000000000, 0.000000000000000000, 1.000000000000000000 ) ) ;
#760=DIRECTION ( 'NONE',  ( 1.000000000000000000, 0.000000000000000000, 0.000000000000000000 ) ) ;
#796=VERTEX_POINT ( 'NONE', #7959 ) ;
#810=DIRECTION ( 'NONE',  ( 0.000000000000000000, 1.000000000000000000, -1.224646799147353207E-16 ) ) ;
#816=ORIENTED_EDGE ( 'NONE', *, *, #11155, .T. ) ;
#860=FACE_OUTER_BOUND ( 'NONE', #1615, .T. ) ;
#914=EDGE_LOOP ( 'NONE', ( #13278, #11223 ) ) ;
#916=AXIS2_PLACEMENT_3D ( 'NONE', #13048, #8314, #2933 ) ;
#941=CARTESIAN_POINT ( 'NONE',  ( -0.1920286436967153787, 0.000000000000000000, 0.000000000000000000 ) ) ;
#1010=ORIENTED_EDGE ( 'NONE', *, *, #4852, .T. ) ;
#1015=AXIS2_PLACEMENT_3D ( 'NONE', #12492, #9399, #452 ) ;
#1030=VERTEX_POINT ( 'NONE', #3210 ) ;
#1058=PRESENTATION_STYLE_ASSIGNMENT (( #12279 ) ) ;
#1083=CARTESIAN_POINT ( 'NONE',  ( 1.399999999999998579, 0.000000000000000000, 0.000000000000000000 ) ) ;
#1098=AXIS2_PLACEMENT_3D ( 'NONE', #169, #2550, #9503 ) ;
#1127=LINE ( 'NONE', #1287, #9270 ) ;
#1132=DIRECTION ( 'NONE',  ( 1.000000000000000000, 0.000000000000000000, 0.000000000000000000 ) ) ;
#1144=DIRECTION ( 'NONE',  ( 1.000000000000000000, 0.000000000000000000, 0.000000000000000000 ) ) ;
#1155=CIRCLE ( 'NONE', #6814, 0.1000000000000002554 ) ;
#1159=CARTESIAN_POINT ( 'NONE',  ( -20.63749999999999929, 0.000000000000000000, 0.000000000000000000 ) ) ;
#1163=AXIS2_PLACEMENT_3D ( 'NONE', #6324, #6111, #1595 ) ;
#1222=CIRCLE ( 'NONE', #741, 0.7499999999999997780 ) ;
#1231=CARTESIAN_POINT ( 'NONE',  ( -1.500000000000001332, 0.000000000000000000, 0.000000000000000000 ) ) ;
#1235=ADVANCED_FACE ( 'NONE', ( #5784, #148 ), #4690, .T. ) ;
#1256=DIRECTION ( 'NONE',  ( 1.000000000000000000, 0.000000000000000000, 0.000000000000000000 ) ) ;
#1287=CARTESIAN_POINT ( 'NONE',  ( -20.63749999999999929, 6.123233995736766282E-16, 5.000000000000000000 ) ) ;
#1291=ORIENTED_EDGE ( 'NONE', *, *, #25, .F. ) ;
#1307=VERTEX_POINT ( 'NONE', #5062 ) ;
#1350=CARTESIAN_POINT ( 'NONE',  ( -1.400000000000000133, 0.000000000000000000, 0.000000000000000000 ) ) ;
#1411=DIRECTION ( 'NONE',  ( 0.000000000000000000, -1.000000000000000000, 0.000000000000000000 ) ) ;
#1418=ORIENTED_EDGE ( 'NONE', *, *, #3188, .T. ) ;
#1419=DIRECTION ( 'NONE',  ( 0.000000000000000000, 0.000000000000000000, 1.000000000000000000 ) ) ;
#1426=AXIS2_PLACEMENT_3D ( 'NONE', #3378, #13189, #7877 ) ;
#1455=DIRECTION ( 'NONE',  ( 0.000000000000000000, 0.000000000000000000, 1.000000000000000000 ) ) ;
#1509=ORIENTED_EDGE ( 'NONE', *, *, #10325, .F. ) ;
#1545=DIRECTION ( 'NONE',  ( 1.000000000000000000, 0.000000000000000000, 0.000000000000000000 ) ) ;
#1562=DIRECTION ( 'NONE',  ( 0.000000000000000000, 0.000000000000000000, -1.000000000000000000 ) ) ;
#1570=EDGE_LOOP ( 'NONE', ( #3192, #9625, #14307, #7227 ) ) ;
#1594=LINE ( 'NONE', #9653, #10816 ) ;
#1595=DIRECTION ( 'NONE',  ( 0.000000000000000000, 0.000000000000000000, -1.000000000000000000 ) ) ;
#1603=PRODUCT_DEFINITION ( 'UNKNOWN', '', #270, #5912 ) ;
#1615=EDGE_LOOP ( 'NONE', ( #3200, #3091, #4348, #1810 ) ) ;
#1619=FACE_OUTER_BOUND ( 'NONE', #2576, .T. ) ;
#1624=ORIENTED_EDGE ( 'NONE', *, *, #13598, .T. ) ;
#1632=CYLINDRICAL_SURFACE ( 'NONE', #9383, 5.525000000000000355 ) ;
#1664=AXIS2_PLACEMENT_3D ( 'NONE', #9751, #13284, #7679 ) ;
#1669=AXIS2_PLACEMENT_3D ( 'NONE', #12242, #5758, #10259 ) ;
#1674=AXIS2_PLACEMENT_3D ( 'NONE', #6769, #13345, #7891 ) ;
#1684=( GEOMETRIC_REPRESENTATION_CONTEXT ( 3 ) GLOBAL_UNCERTAINTY_ASSIGNED_CONTEXT ( ( #4141 ) ) GLOBAL_UNIT_ASSIGNED_CONTEXT ( ( #7997, #12353, #5509 ) ) REPRESENTATION_CONTEXT ( 'NONE', 'WORKASPACE' ) );
#1698=ORIENTED_EDGE ( 'NONE', *, *, #12361, .T. ) ;
#1712=CIRCLE ( 'NONE', #2179, 5.525000000000000355 ) ;
#1739=CARTESIAN_POINT ( 'NONE',  ( -1.500000000000001332, 0.000000000000000000, 0.000000000000000000 ) ) ;
#1761=CARTESIAN_POINT ( 'NONE',  ( -1.500000000000001332, 0.000000000000000000, 0.000000000000000000 ) ) ;
#1803=CARTESIAN_POINT ( 'NONE',  ( 0.1920286436967153787, 7.516269729766880368E-16, -5.525000000000000355 ) ) ;
#1810=ORIENTED_EDGE ( 'NONE', *, *, #2803, .F. ) ;
#1835=EDGE_CURVE ( 'NONE', #8255, #6536, #14349, .T. ) ;
#1890=EDGE_LOOP ( 'NONE', ( #7121, #1010, #6690, #9370 ) ) ;
#1899=DIRECTION ( 'NONE',  ( 1.000000000000000000, 0.000000000000000000, 0.000000000000000000 ) ) ;
#1956=ORIENTED_EDGE ( 'NONE', *, *, #5983, .T. ) ;
#1965=CIRCLE ( 'NONE', #3861, 0.1000000000000002554 ) ;
#1982=ORIENTED_EDGE ( 'NONE', *, *, #13598, .F. ) ;
#2022=EDGE_LOOP ( 'NONE', ( #9325, #14476, #4318, #8173 ) ) ;
#2051=ORIENTED_EDGE ( 'NONE', *, *, #3376, .T. ) ;
#2080=LINE ( 'NONE', #14564, #5664 ) ;
#2093=ORIENTED_EDGE ( 'NONE', *, *, #10269, .F. ) ;
#2109=AXIS2_PLACEMENT_3D ( 'NONE', #7802, #10011, #8684 ) ;
#2163=TOROIDAL_SURFACE ( 'NONE', #10671, 5.100000000000000533, 0.1000000000000001582 ) ;
#2170=MANIFOLD_SOLID_BREP ( 'OuterRace', #9516 ) ;
#2173=( NAMED_UNIT ( * ) PLANE_ANGLE_UNIT ( ) SI_UNIT ( $, .RADIAN. ) );
#2179=AXIS2_PLACEMENT_3D ( 'NONE', #7051, #11556, #1455 ) ;
#2188=DIRECTION ( 'NONE',  ( 1.000000000000000000, 0.000000000000000000, 0.000000000000000000 ) ) ;
#2216=DIRECTION ( 'NONE',  ( 0.000000000000000000, 1.000000000000000000, -1.224646799147353207E-16 ) ) ;
#2228=EDGE_CURVE ( 'NONE', #1307, #3448, #11946, .T. ) ;
#2254=EDGE_LOOP ( 'NONE', ( #8971, #12568, #816, #1418 ) ) ;
#2279=DIRECTION ( 'NONE',  ( 1.000000000000000000, 0.000000000000000000, 0.000000000000000000 ) ) ;
#2291=VERTEX_POINT ( 'NONE', #12735 ) ;
#2323=CARTESIAN_POINT ( 'NONE',  ( 1.500000000000001332, 0.000000000000000000, 0.000000000000000000 ) ) ;
#2332=AXIS2_PLACEMENT_3D ( 'NONE', #201, #9308, #13809 ) ;
#2380=CARTESIAN_POINT ( 'NONE',  ( -20.63749999999999929, 0.000000000000000000, 0.000000000000000000 ) ) ;
#2401=EDGE_CURVE ( 'NONE', #13831, #796, #7013, .T. ) ;
#2409=ORIENTED_EDGE ( 'NONE', *, *, #13249, .F. ) ;
#2463=DIRECTION ( 'NONE',  ( 0.000000000000000000, 0.000000000000000000, -1.000000000000000000 ) ) ;
#2528=ADVANCED_FACE ( 'NONE', ( #13148 ), #1632, .T. ) ;
#2550=DIRECTION ( 'NONE',  ( 1.000000000000000000, 0.000000000000000000, 0.000000000000000000 ) ) ;
#2560=EDGE_CURVE ( 'NONE', #3448, #1307, #5845, .T. ) ;
#2576=EDGE_LOOP ( 'NONE', ( #5534, #12423, #9463, #524 ) ) ;
#2590=EDGE_CURVE ( 'NONE', #442, #12943, #11031, .T. ) ;
#2594=AXIS2_PLACEMENT_3D ( 'NONE', #11900, #8660, #3136 ) ;
#2629=EDGE_CURVE ( 'NONE', #4733, #2291, #2662, .T. ) ;
#2662=LINE ( 'NONE', #56, #6794 ) ;
#2666=DIRECTION ( 'NONE',  ( 0.000000000000000000, 0.000000000000000000, 1.000000000000000000 ) ) ;
#2688=DIRECTION ( 'NONE',  ( -1.000000000000000000, 0.000000000000000000, -0.000000000000000000 ) ) ;
#2742=EDGE_CURVE ( 'NONE', #12153, #8153, #4069, .T. ) ;
#2798=CARTESIAN_POINT ( 'NONE',  ( -20.63749999999999574, 8.541911424052788811E-16, 6.975000000000000533 ) ) ;
#2803=EDGE_CURVE ( 'NONE', #2876, #5286, #8686, .T. ) ;
#2846=CIRCLE ( 'NONE', #4507, 7.399999999999999467 ) ;
#2854=EDGE_CURVE ( 'NONE', #5286, #2876, #10335, .T. ) ;
#2874=CIRCLE ( 'NONE', #13482, 7.399999999999999467 ) ;
#2876=VERTEX_POINT ( 'NONE', #8782 ) ;
#2879=ORIENTED_EDGE ( 'NONE', *, *, #1835, .T. ) ;
#2910=CARTESIAN_POINT ( 'NONE',  ( -1.400000000000000133, 6.245698675651501825E-16, 5.100000000000000533 ) ) ;
#2916=ORIENTED_EDGE ( 'NONE', *, *, #13451, .T. ) ;
#2933=DIRECTION ( 'NONE',  ( 0.000000000000000000, 0.000000000000000000, -1.000000000000000000 ) ) ;
#2941=DIRECTION ( 'NONE',  ( 1.000000000000000000, 0.000000000000000000, 0.000000000000000000 ) ) ;
#2951=DIRECTION ( 'NONE',  ( 1.000000000000000000, 0.000000000000000000, 0.000000000000000000 ) ) ;
#2982=CYLINDRICAL_SURFACE ( 'NONE', #12965, 7.500000000000000000 ) ;
#2991=CARTESIAN_POINT ( 'NONE',  ( 0.000000000000000000, 0.000000000000000000, 6.250000000000000000 ) ) ;
#3010=( GEOMETRIC_REPRESENTATION_CONTEXT ( 3 ) GLOBAL_UNCERTAINTY_ASSIGNED_CONTEXT ( ( #7693 ) ) GLOBAL_UNIT_ASSIGNED_CONTEXT ( ( #8397, #13801, #13954 ) ) REPRESENTATION_CONTEXT ( 'NONE', 'WORKASPACE' ) );
#3039=CARTESIAN_POINT ( 'NONE',  ( -20.63749999999999929, 0.000000000000000000, 0.000000000000000000 ) ) ;
#3055=AXIS2_PLACEMENT_3D ( 'NONE', #10999, #2279, #11295 ) ;
#3056=DIRECTION ( 'NONE',  ( 0.000000000000000000, 0.000000000000000000, -1.000000000000000000 ) ) ;
#3066=EDGE_CURVE ( 'NONE', #1307, #11290, #1594, .T. ) ;
#3078=AXIS2_PLACEMENT_3D ( 'NONE', #4098, #8426, #753 ) ;
#3091=ORIENTED_EDGE ( 'NONE', *, *, #3679, .T. ) ;
#3094=ORIENTED_EDGE ( 'NONE', *, *, #7350, .T. ) ;
#3103=CIRCLE ( 'NONE', #14408, 7.399999999999999467 ) ;
#3136=DIRECTION ( 'NONE',  ( 0.000000000000000000, 0.000000000000000000, 1.000000000000000000 ) ) ;
#3163=VERTEX_POINT ( 'NONE', #6738 ) ;
#3186=VERTEX_POINT ( 'NONE', #11096 ) ;
#3188=EDGE_CURVE ( 'NONE', #8553, #5688, #9875, .T. ) ;
#3191=CARTESIAN_POINT ( 'NONE',  ( 1.399999999999999689, 9.062386313690412402E-16, 7.399999999999999467 ) ) ;
#3192=ORIENTED_EDGE ( 'NONE', *, *, #12327, .F. ) ;
#3200=ORIENTED_EDGE ( 'NONE', *, *, #12553, .F. ) ;
#3201=ORIENTED_EDGE ( 'NONE', *, *, #12327, .T. ) ;
#3210=CARTESIAN_POINT ( 'NONE',  ( 1.500000000000001332, 8.266365894244634333E-16, 6.750000000000000000 ) ) ;
#3225=CARTESIAN_POINT ( 'NONE',  ( -0.5590169943749470072, 0.000000000000000000, 0.000000000000000000 ) ) ;
#3285=FILL_AREA_STYLE_COLOUR ( '', #10178 ) ;
#3287=CYLINDRICAL_SURFACE ( 'NONE', #697, 5.750000000000000000 ) ;
#3292=ORIENTED_EDGE ( 'NONE', *, *, #10269, .T. ) ;
#3294=AXIS2_PLACEMENT_3D ( 'NONE', #7464, #530, #1562 ) ;
#3323=AXIS2_PLACEMENT_3D ( 'NONE', #4885, #13882, #2666 ) ;
#3347=EDGE_LOOP ( 'NONE', ( #12243, #4572 ) ) ;
#3376=EDGE_CURVE ( 'NONE', #13812, #1030, #11050, .T. ) ;
#3378=CARTESIAN_POINT ( 'NONE',  ( 1.500000000000001332, 0.000000000000000000, 0.000000000000000000 ) ) ;
#3380=ORIENTED_EDGE ( 'NONE', *, *, #10973, .F. ) ;
#3444=CARTESIAN_POINT ( 'NONE',  ( -20.63749999999999929, 0.000000000000000000, 0.000000000000000000 ) ) ;
#3448=VERTEX_POINT ( 'NONE', #5053 ) ;
#3452=PRODUCT_DEFINITION_SHAPE ( 'NONE', 'NONE',  #1603 ) ;
#3500=PLANE ( 'NONE',  #5595 ) ;
#3529=CIRCLE ( 'NONE', #5415, 7.399999999999999467 ) ;
#3587=CARTESIAN_POINT ( 'NONE',  ( 1.500000000000000444, 5.100000000000000533, 0.000000000000000000 ) ) ;
#3604=DIRECTION ( 'NONE',  ( 0.000000000000000000, 0.000000000000000000, -1.000000000000000000 ) ) ;
#3605=DIRECTION ( 'NONE',  ( 0.000000000000000000, 0.000000000000000000, -1.000000000000000000 ) ) ;
#3661=CARTESIAN_POINT ( 'NONE',  ( -1.399999999999999689, 0.000000000000000000, 0.000000000000000000 ) ) ;
#3665=DIRECTION ( 'NONE',  ( 0.000000000000000000, 0.000000000000000000, -1.000000000000000000 ) ) ;
#3679=EDGE_CURVE ( 'NONE', #5458, #6536, #10116, .T. ) ;
#3724=CARTESIAN_POINT ( 'NONE',  ( -1.499999999999999556, 6.975000000000000533, 0.000000000000000000 ) ) ;
#3737=EDGE_CURVE ( 'NONE', #8153, #5571, #9884, .T. ) ;
#3781=SHAPE_REPRESENTATION ( 'angular contact ball bearing_68_iso_ISO 15 ABB - 1710 - 20,SI,NC,20_68', ( #9440 ), #10888 ) ;
#3811=AXIS2_PLACEMENT_3D ( 'NONE', #941, #14467, #8631 ) ;
#3856=EDGE_CURVE ( 'NONE', #5068, #12967, #1155, .T. ) ;
#3861=AXIS2_PLACEMENT_3D ( 'NONE', #2910, #13903, #7327 ) ;
#3939=CARTESIAN_POINT ( 'NONE',  ( 1.499999999999999778, 7.399999999999999467, 0.000000000000000000 ) ) ;
#3943=EDGE_CURVE ( 'NONE', #689, #8255, #3529, .T. ) ;
#3962=ADVANCED_FACE ( 'NONE', ( #4498 ), #4574, .T. ) ;
#3969=DIRECTION ( 'NONE',  ( 1.000000000000000000, 0.000000000000000000, 0.000000000000000000 ) ) ;
#4002=VERTEX_POINT ( 'NONE', #8997 ) ;
#4007=CIRCLE ( 'NONE', #9886, 5.750000000000000000 ) ;
#4022=FACE_OUTER_BOUND ( 'NONE', #13986, .T. ) ;
#4030=CARTESIAN_POINT ( 'NONE',  ( -1.500000000000001332, 0.000000000000000000, -6.975000000000000533 ) ) ;
#4031=CARTESIAN_POINT ( 'NONE',  ( -0.1920286436967153787, 0.000000000000000000, 0.000000000000000000 ) ) ;
#4069=LINE ( 'NONE', #2798, #4694 ) ;
#4084=ADVANCED_FACE ( 'NONE', ( #860 ), #14604, .T. ) ;
#4098=CARTESIAN_POINT ( 'NONE',  ( 0.000000000000000000, 0.000000000000000000, 0.000000000000000000 ) ) ;
#4126=EDGE_CURVE ( 'NONE', #6460, #5688, #5193, .T. ) ;
#4132=CARTESIAN_POINT ( 'NONE',  ( -1.500000000000001332, 0.000000000000000000, 0.000000000000000000 ) ) ;
#4134=EDGE_CURVE ( 'NONE', #6460, #442, #10528, .T. ) ;
#4141=UNCERTAINTY_MEASURE_WITH_UNIT (LENGTH_MEASURE( 1.000000000000000082E-05 ), #7997, 'distance_accuracy_value', 'NONE');
#4151=ORIENTED_EDGE ( 'NONE', *, *, #4848, .F. ) ;
#4157=ADVANCED_FACE ( 'NONE', ( #10467 ), #9357, .F. ) ;
#4165=FACE_OUTER_BOUND ( 'NONE', #10413, .T. ) ;
#4190=DIRECTION ( 'NONE',  ( 0.000000000000000000, 0.000000000000000000, -1.000000000000000000 ) ) ;
#4264=CARTESIAN_POINT ( 'NONE',  ( -1.400000000000001910, 6.123233995736766282E-16, 5.000000000000000000 ) ) ;
#4287=CARTESIAN_POINT ( 'NONE',  ( -1.400000000000001910, 0.000000000000000000, -5.000000000000000000 ) ) ;
#4290=ADVANCED_FACE ( 'NONE', ( #11700 ), #686, .T. ) ;
#4296=VERTEX_POINT ( 'NONE', #8317 ) ;
#4313=CARTESIAN_POINT ( 'NONE',  ( -20.63749999999999574, 9.184850993605147944E-16, 7.500000000000000000 ) ) ;
#4318=ORIENTED_EDGE ( 'NONE', *, *, #12783, .T. ) ;
#4347=CARTESIAN_POINT ( 'NONE',  ( 0.000000000000000000, 0.000000000000000000, 0.000000000000000000 ) ) ;
#4348=ORIENTED_EDGE ( 'NONE', *, *, #11146, .T. ) ;
#4354=CARTESIAN_POINT ( 'NONE',  ( -20.63749999999999574, 0.000000000000000000, 0.000000000000000000 ) ) ;
#4362=ORIENTED_EDGE ( 'NONE', *, *, #12248, .F. ) ;
#4369=DIRECTION ( 'NONE',  ( 1.000000000000000000, 0.000000000000000000, 0.000000000000000000 ) ) ;
#4394=SURFACE_SIDE_STYLE ('',( #13610 ) ) ;
#4409=EDGE_CURVE ( 'NONE', #6536, #5458, #4474, .T. ) ;
#4465=( NAMED_UNIT ( * ) SI_UNIT ( $, .STERADIAN. ) SOLID_ANGLE_UNIT ( ) );
#4474=CIRCLE ( 'NONE', #2109, 7.500000000000000000 ) ;
#4483=DIRECTION ( 'NONE',  ( 1.000000000000000000, 0.000000000000000000, 0.000000000000000000 ) ) ;
#4484=CIRCLE ( 'NONE', #13257, 0.1000000000000002554 ) ;
#4498=FACE_OUTER_BOUND ( 'NONE', #62, .T. ) ;
#4501=EDGE_CURVE ( 'NONE', #13831, #5068, #7311, .T. ) ;
#4507=AXIS2_PLACEMENT_3D ( 'NONE', #8487, #5171, #9596 ) ;
#4513=PRODUCT_CONTEXT ( 'NONE', #11586, 'mechanical' ) ;
#4518=VERTEX_POINT ( 'NONE', #4264 ) ;
#4541=CYLINDRICAL_SURFACE ( 'NONE', #6152, 6.975000000000000533 ) ;
#4564=ORIENTED_EDGE ( 'NONE', *, *, #10973, .T. ) ;
#4572=ORIENTED_EDGE ( 'NONE', *, *, #2560, .F. ) ;
#4574=CYLINDRICAL_SURFACE ( 'NONE', #11524, 5.525000000000000355 ) ;
#4602=EDGE_CURVE ( 'NONE', #12967, #796, #11315, .T. ) ;
#4612=DIRECTION ( 'NONE',  ( 1.000000000000000000, 0.000000000000000000, 0.000000000000000000 ) ) ;
#4620=FILL_AREA_STYLE ('',( #3285 ) ) ;
#4678=CYLINDRICAL_SURFACE ( 'NONE', #10883, 5.750000000000000000 ) ;
#4688=DIRECTION ( 'NONE',  ( 1.000000000000000000, 0.000000000000000000, 0.000000000000000000 ) ) ;
#4690=PLANE ( 'NONE',  #11724 ) ;
#4694=VECTOR ( 'NONE', #2951, 1000.000000000000000 ) ;
#4705=AXIS2_PLACEMENT_3D ( 'NONE', #12713, #6148, #8353 ) ;
#4725=EDGE_LOOP ( 'NONE', ( #5446, #12549 ) ) ;
#4733=VERTEX_POINT ( 'NONE', #4030 ) ;
#4748=AXIS2_PLACEMENT_3D ( 'NONE', #10484, #14099, #12848 ) ;
#4792=AXIS2_PLACEMENT_3D ( 'NONE', #3444, #7943, #10087 ) ;
#4798=CARTESIAN_POINT ( 'NONE',  ( -20.63749999999999929, 6.766173565289127388E-16, 5.525000000000000355 ) ) ;
#4804=EDGE_LOOP ( 'NONE', ( #3380, #13487 ) ) ;
#4848=EDGE_CURVE ( 'NONE', #8553, #1030, #2080, .T. ) ;
#4849=CARTESIAN_POINT ( 'NONE',  ( 1.400000000000001910, 0.000000000000000000, 0.000000000000000000 ) ) ;
#4852=EDGE_CURVE ( 'NONE', #4518, #10329, #223, .T. ) ;
#4885=CARTESIAN_POINT ( 'NONE',  ( 0.1920286436967153787, 0.000000000000000000, 0.000000000000000000 ) ) ;
#4930=FACE_OUTER_BOUND ( 'NONE', #1890, .T. ) ;
#4964=CARTESIAN_POINT ( 'NONE',  ( 1.500000000000001332, 0.000000000000000000, -5.525000000000000355 ) ) ;
#4965=ORIENTED_EDGE ( 'NONE', *, *, #4602, .T. ) ;
#4967=DIRECTION ( 'NONE',  ( 0.000000000000000000, -1.000000000000000000, 0.000000000000000000 ) ) ;
#4984=FACE_OUTER_BOUND ( 'NONE', #11870, .T. ) ;
#4993=DIRECTION ( 'NONE',  ( 1.000000000000000000, 0.000000000000000000, 0.000000000000000000 ) ) ;
#5013=ADVANCED_FACE ( 'NONE', ( #1619 ), #4541, .F. ) ;
#5035=DIRECTION ( 'NONE',  ( 0.000000000000000000, 0.000000000000000000, -1.000000000000000000 ) ) ;
#5053=CARTESIAN_POINT ( 'NONE',  ( -1.500000000000001332, 7.041719095097280880E-16, 5.750000000000000000 ) ) ;
#5062=CARTESIAN_POINT ( 'NONE',  ( -1.500000000000001332, 0.000000000000000000, -5.750000000000000000 ) ) ;
#5068=VERTEX_POINT ( 'NONE', #13132 ) ;
#5082=EDGE_LOOP ( 'NONE', ( #10308, #7471, #13099, #8772 ) ) ;
#5097=ORIENTED_EDGE ( 'NONE', *, *, #4501, .F. ) ;
#5141=CYLINDRICAL_SURFACE ( 'NONE', #10911, 6.975000000000000533 ) ;
#5171=DIRECTION ( 'NONE',  ( 1.000000000000000000, 0.000000000000000000, 0.000000000000000000 ) ) ;
#5175=ORIENTED_EDGE ( 'NONE', *, *, #14089, .T. ) ;
#5176=CARTESIAN_POINT ( 'NONE',  ( -1.399999999999999689, 0.000000000000000000, -7.399999999999999467 ) ) ;
#5187=TOROIDAL_SURFACE ( 'NONE', #10134, 7.399999999999999467, 0.1000000000000000472 ) ;
#5193=CIRCLE ( 'NONE', #8008, 0.7499999999999997780 ) ;
#5225=ADVANCED_FACE ( 'NONE', ( #8847 ), #6564, .F. ) ;
#5251=CARTESIAN_POINT ( 'NONE',  ( 1.400000000000000133, 0.000000000000000000, -5.100000000000000533 ) ) ;
#5273=ORIENTED_EDGE ( 'NONE', *, *, #11797, .F. ) ;
#5286=VERTEX_POINT ( 'NONE', #13283 ) ;
#5287=CARTESIAN_POINT ( 'NONE',  ( -20.63749999999999574, 0.000000000000000000, -7.500000000000000000 ) ) ;
#5415=AXIS2_PLACEMENT_3D ( 'NONE', #1761, #6266, #8846 ) ;
#5416=CARTESIAN_POINT ( 'NONE',  ( -1.400000000000000133, 0.000000000000000000, -5.100000000000000533 ) ) ;
#5424=DIRECTION ( 'NONE',  ( 1.000000000000000000, 0.000000000000000000, 0.000000000000000000 ) ) ;
#5446=ORIENTED_EDGE ( 'NONE', *, *, #13336, .T. ) ;
#5458=VERTEX_POINT ( 'NONE', #7282 ) ;
#5459=DIRECTION ( 'NONE',  ( 0.000000000000000000, 0.000000000000000000, -1.000000000000000000 ) ) ;
#5489=DIRECTION ( 'NONE',  ( 0.000000000000000000, 0.000000000000000000, -1.000000000000000000 ) ) ;
#5492=ORIENTED_EDGE ( 'NONE', *, *, #13336, .F. ) ;
#5508=CARTESIAN_POINT ( 'NONE',  ( 0.1920286436967153787, 0.000000000000000000, 5.525000000000000355 ) ) ;
#5509=( NAMED_UNIT ( * ) SI_UNIT ( $, .STERADIAN. ) SOLID_ANGLE_UNIT ( ) );
#5534=ORIENTED_EDGE ( 'NONE', *, *, #13630, .F. ) ;
#5557=DIRECTION ( 'NONE',  ( 1.000000000000000000, 0.000000000000000000, 0.000000000000000000 ) ) ;
#5563=CARTESIAN_POINT ( 'NONE',  ( -1.399999999999999689, 9.062386313690412402E-16, 7.399999999999999467 ) ) ;
#5571=VERTEX_POINT ( 'NONE', #7587 ) ;
#5595=AXIS2_PLACEMENT_3D ( 'NONE', #3587, #13608, #2463 ) ;
#5605=SHAPE_DEFINITION_REPRESENTATION ( #3452, #3781 ) ;
#5664=VECTOR ( 'NONE', #5424, 1000.000000000000000 ) ;
#5672=DIRECTION ( 'NONE',  ( 0.000000000000000000, 0.000000000000000000, -1.000000000000000000 ) ) ;
#5688=VERTEX_POINT ( 'NONE', #12206 ) ;
#5693=DIRECTION ( 'NONE',  ( 1.000000000000000000, 0.000000000000000000, 0.000000000000000000 ) ) ;
#5702=DIRECTION ( 'NONE',  ( 1.000000000000000000, 0.000000000000000000, 0.000000000000000000 ) ) ;
#5703=AXIS2_PLACEMENT_3D ( 'NONE', #11104, #4688, #8960 ) ;
#5712=EDGE_LOOP ( 'NONE', ( #11916, #7838, #2879, #6900 ) ) ;
#5758=DIRECTION ( 'NONE',  ( 1.000000000000000000, 0.000000000000000000, 0.000000000000000000 ) ) ;
#5759=ORIENTED_EDGE ( 'NONE', *, *, #4602, .F. ) ;
#5780=EDGE_LOOP ( 'NONE', ( #4362, #8331, #3094, #4965 ) ) ;
#5784=FACE_OUTER_BOUND ( 'NONE', #8055, .T. ) ;
#5822=EDGE_LOOP ( 'NONE', ( #11306, #12689, #10139, #13309 ) ) ;
#5826=CIRCLE ( 'NONE', #1098, 5.100000000000000533 ) ;
#5845=CIRCLE ( 'NONE', #7493, 5.750000000000000000 ) ;
#5881=ORIENTED_EDGE ( 'NONE', *, *, #4409, .T. ) ;
#5883=CARTESIAN_POINT ( 'NONE',  ( 0.000000000000000000, 7.654042494670957606E-16, -6.250000000000000000 ) ) ;
#5900=AXIS2_PLACEMENT_3D ( 'NONE', #13011, #10868, #660 ) ;
#5912=PRODUCT_DEFINITION_CONTEXT ( 'detailed design', #13660, 'design' ) ;
#5925=DIRECTION ( 'NONE',  ( -1.000000000000000000, -0.000000000000000000, -0.000000000000000000 ) ) ;
#5938=FACE_BOUND ( 'NONE', #4725, .T. ) ;
#5956=DIRECTION ( 'NONE',  ( 0.000000000000000000, 0.000000000000000000, -1.000000000000000000 ) ) ;
#5983=EDGE_CURVE ( 'NONE', #2291, #8153, #11705, .T. ) ;
#6008=FACE_OUTER_BOUND ( 'NONE', #5712, .T. ) ;
#6022=CARTESIAN_POINT ( 'NONE',  ( -20.63749999999999574, 0.000000000000000000, 0.000000000000000000 ) ) ;
#6039=ORIENTED_EDGE ( 'NONE', *, *, #3856, .F. ) ;
#6045=ADVANCED_FACE ( 'NONE', ( #294 ), #13366, .T. ) ;
#6086=AXIS2_PLACEMENT_3D ( 'NONE', #9764, #810, #6146 ) ;
#6095=AXIS2_PLACEMENT_3D ( 'NONE', #9960, #14462, #12376 ) ;
#6099=DIRECTION ( 'NONE',  ( 0.000000000000000000, 0.000000000000000000, -1.000000000000000000 ) ) ;
#6111=DIRECTION ( 'NONE',  ( 1.000000000000000000, 0.000000000000000000, 0.000000000000000000 ) ) ;
#6121=AXIS2_PLACEMENT_3D ( 'NONE', #10754, #1899, #4190 ) ;
#6139=DIRECTION ( 'NONE',  ( 0.000000000000000000, 0.000000000000000000, -1.000000000000000000 ) ) ;
#6146=DIRECTION ( 'NONE',  ( 0.000000000000000000, 1.224646799147353207E-16, 1.000000000000000000 ) ) ;
#6148=DIRECTION ( 'NONE',  ( 1.000000000000000000, 0.000000000000000000, 0.000000000000000000 ) ) ;
#6152=AXIS2_PLACEMENT_3D ( 'NONE', #12409, #4612, #13679 ) ;
#6256=FACE_BOUND ( 'NONE', #7681, .T. ) ;
#6261=DIRECTION ( 'NONE',  ( 1.000000000000000000, 0.000000000000000000, 0.000000000000000000 ) ) ;
#6266=DIRECTION ( 'NONE',  ( 1.000000000000000000, 0.000000000000000000, 0.000000000000000000 ) ) ;
#6281=EDGE_CURVE ( 'NONE', #5068, #13831, #5826, .T. ) ;
#6302=MECHANICAL_DESIGN_GEOMETRIC_PRESENTATION_REPRESENTATION('',(#13365),#3010);
#6308=CIRCLE ( 'NONE', #14556, 5.525000000000000355 ) ;
#6324=CARTESIAN_POINT ( 'NONE',  ( 1.400000000000000133, 0.000000000000000000, 0.000000000000000000 ) ) ;
#6355=TOROIDAL_SURFACE ( 'NONE', #916, 5.100000000000000533, 0.1000000000000001582 ) ;
#6375=FACE_OUTER_BOUND ( 'NONE', #6687, .T. ) ;
#6405=ORIENTED_EDGE ( 'NONE', *, *, #2854, .F. ) ;
#6415=CARTESIAN_POINT ( 'NONE',  ( -1.500000000000000444, 5.750000000000000000, 0.000000000000000000 ) ) ;
#6417=DIRECTION ( 'NONE',  ( 1.000000000000000000, 0.000000000000000000, 0.000000000000000000 ) ) ;
#6451=CIRCLE ( 'NONE', #1015, 5.100000000000000533 ) ;
#6460=VERTEX_POINT ( 'NONE', #1803 ) ;
#6468=DIRECTION ( 'NONE',  ( 1.000000000000000000, 0.000000000000000000, 0.000000000000000000 ) ) ;
#6524=EDGE_LOOP ( 'NONE', ( #640, #5097 ) ) ;
#6536=VERTEX_POINT ( 'NONE', #9182 ) ;
#6548=ADVANCED_FACE ( 'NONE', ( #8884, #13688 ), #3500, .T. ) ;
#6560=AXIS2_PLACEMENT_3D ( 'NONE', #6940, #1545, #6868 ) ;
#6564=CYLINDRICAL_SURFACE ( 'NONE', #1674, 5.000000000000000000 ) ;
#6601=DIRECTION ( 'NONE',  ( 1.000000000000000000, 0.000000000000000000, 0.000000000000000000 ) ) ;
#6623=CIRCLE ( 'NONE', #3811, 6.975000000000000533 ) ;
#6649=ORIENTED_EDGE ( 'NONE', *, *, #4134, .T. ) ;
#6666=CIRCLE ( 'NONE', #8547, 0.7499999999999997780 ) ;
#6687=EDGE_LOOP ( 'NONE', ( #4564, #5175, #10919, #9794 ) ) ;
#6690=ORIENTED_EDGE ( 'NONE', *, *, #7862, .T. ) ;
#6721=FACE_OUTER_BOUND ( 'NONE', #7968, .T. ) ;
#6738=CARTESIAN_POINT ( 'NONE',  ( -1.500000000000000888, 0.000000000000000000, -5.100000000000000533 ) ) ;
#6742=FACE_OUTER_BOUND ( 'NONE', #2022, .T. ) ;
#6769=CARTESIAN_POINT ( 'NONE',  ( -20.63749999999999929, 0.000000000000000000, 0.000000000000000000 ) ) ;
#6789=CARTESIAN_POINT ( 'NONE',  ( -1.500000000000001332, 0.000000000000000000, 0.000000000000000000 ) ) ;
#6794=VECTOR ( 'NONE', #9081, 1000.000000000000000 ) ;
#6811=EDGE_LOOP ( 'NONE', ( #5273, #1956, #12170, #13731 ) ) ;
#6813=DIRECTION ( 'NONE',  ( 0.000000000000000000, 1.000000000000000000, -1.224646799147353207E-16 ) ) ;
#6814=AXIS2_PLACEMENT_3D ( 'NONE', #5251, #11719, #5035 ) ;
#6868=DIRECTION ( 'NONE',  ( 0.000000000000000000, 0.000000000000000000, -1.000000000000000000 ) ) ;
#6897=DIRECTION ( 'NONE',  ( 1.000000000000000000, 0.000000000000000000, 0.000000000000000000 ) ) ;
#6900=ORIENTED_EDGE ( 'NONE', *, *, #3679, .F. ) ;
#6901=CARTESIAN_POINT ( 'NONE',  ( -20.63749999999999929, 0.000000000000000000, 0.000000000000000000 ) ) ;
#6902=ORIENTED_EDGE ( 'NONE', *, *, #10325, .T. ) ;
#6903=ORIENTED_EDGE ( 'NONE', *, *, #407, .F. ) ;
#6922=ADVANCED_FACE ( 'NONE', ( #6375 ), #8220, .T. ) ;
#6940=CARTESIAN_POINT ( 'NONE',  ( 1.500000000000001332, 0.000000000000000000, 0.000000000000000000 ) ) ;
#7013=CIRCLE ( 'NONE', #6086, 0.1000000000000002554 ) ;
#7026=AXIS2_PLACEMENT_3D ( 'NONE', #1083, #10022, #5459 ) ;
#7051=CARTESIAN_POINT ( 'NONE',  ( 0.1920286436967153787, 0.000000000000000000, 0.000000000000000000 ) ) ;
#7078=CIRCLE ( 'NONE', #1669, 5.100000000000000533 ) ;
#7090=DIRECTION ( 'NONE',  ( 1.000000000000000000, 0.000000000000000000, 0.000000000000000000 ) ) ;
#7121=ORIENTED_EDGE ( 'NONE', *, *, #31, .F. ) ;
#7176=CARTESIAN_POINT ( 'NONE',  ( 0.000000000000000000, 0.000000000000000000, 0.000000000000000000 ) ) ;
#7186=DIRECTION ( 'NONE',  ( 0.000000000000000000, 0.000000000000000000, -1.000000000000000000 ) ) ;
#7202=DIRECTION ( 'NONE',  ( 1.000000000000000000, 0.000000000000000000, 0.000000000000000000 ) ) ;
#7210=CARTESIAN_POINT ( 'NONE',  ( -20.63749999999999929, 0.000000000000000000, -5.000000000000000000 ) ) ;
#7211=ORIENTED_EDGE ( 'NONE', *, *, #8372, .T. ) ;
#7227=ORIENTED_EDGE ( 'NONE', *, *, #9551, .F. ) ;
#7282=CARTESIAN_POINT ( 'NONE',  ( -1.399999999999998579, 9.184850993605147944E-16, 7.500000000000000000 ) ) ;
#7296=ORIENTED_EDGE ( 'NONE', *, *, #2629, .T. ) ;
#7311=CIRCLE ( 'NONE', #1426, 5.100000000000000533 ) ;
#7327=DIRECTION ( 'NONE',  ( 0.000000000000000000, 1.224646799147353207E-16, 1.000000000000000000 ) ) ;
#7350=EDGE_CURVE ( 'NONE', #10329, #12967, #11559, .T. ) ;
#7384=ADVANCED_FACE ( 'NONE', ( #4930 ), #6355, .T. ) ;
#7420=DIRECTION ( 'NONE',  ( -1.000000000000000000, -0.000000000000000000, -0.000000000000000000 ) ) ;
#7464=CARTESIAN_POINT ( 'NONE',  ( -1.500000000000001332, 0.000000000000000000, 0.000000000000000000 ) ) ;
#7471=ORIENTED_EDGE ( 'NONE', *, *, #12248, .T. ) ;
#7488=DIRECTION ( 'NONE',  ( 0.000000000000000000, -1.000000000000000000, 0.000000000000000000 ) ) ;
#7493=AXIS2_PLACEMENT_3D ( 'NONE', #6789, #5693, #8718 ) ;
#7504=CIRCLE ( 'NONE', #9396, 0.1000000000000002554 ) ;
#7509=DIRECTION ( 'NONE',  ( -0.000000000000000000, 1.000000000000000000, 1.224646799147353207E-16 ) ) ;
#7529=ADVANCED_FACE ( 'NONE', ( #8077 ), #3287, .T. ) ;
#7587=CARTESIAN_POINT ( 'NONE',  ( -0.5590169943749470072, 7.041719095097280880E-16, 5.750000000000000000 ) ) ;
#7628=DIRECTION ( 'NONE',  ( 0.000000000000000000, 1.224646799147343593E-16, 1.000000000000000000 ) ) ;
#7631=CARTESIAN_POINT ( 'NONE',  ( -20.63749999999999574, 0.000000000000000000, -6.750000000000000000 ) ) ;
#7650=ADVANCED_FACE ( 'NONE', ( #6008 ), #5187, .T. ) ;
#7679=DIRECTION ( 'NONE',  ( 0.000000000000000000, 0.000000000000000000, -1.000000000000000000 ) ) ;
#7681=EDGE_LOOP ( 'NONE', ( #13753, #7211 ) ) ;
#7683=DIRECTION ( 'NONE',  ( 0.000000000000000000, 0.000000000000000000, 1.000000000000000000 ) ) ;
#7693=UNCERTAINTY_MEASURE_WITH_UNIT (LENGTH_MEASURE( 1.000000000000000082E-05 ), #8397, 'distance_accuracy_value', 'NONE');
#7705=CARTESIAN_POINT ( 'NONE',  ( 0.5590169943749477843, 0.000000000000000000, 0.000000000000000000 ) ) ;
#7735=ORIENTED_EDGE ( 'NONE', *, *, #3066, .F. ) ;
#7752=VECTOR ( 'NONE', #7771, 1000.000000000000000 ) ;
#7759=DIRECTION ( 'NONE',  ( 0.000000000000000000, 0.000000000000000000, -1.000000000000000000 ) ) ;
#7771=DIRECTION ( 'NONE',  ( 1.000000000000000000, 0.000000000000000000, 0.000000000000000000 ) ) ;
#7776=CIRCLE ( 'NONE', #3294, 6.975000000000000533 ) ;
#7785=ADVANCED_FACE ( 'NONE', ( #4165 ), #8954, .T. ) ;
#7793=ORIENTED_EDGE ( 'NONE', *, *, #7862, .F. ) ;
#7802=CARTESIAN_POINT ( 'NONE',  ( -1.399999999999998579, 0.000000000000000000, 0.000000000000000000 ) ) ;
#7832=ADVANCED_FACE ( 'NONE', ( #4022 ), #2982, .T. ) ;
#7834=FACE_OUTER_BOUND ( 'NONE', #2254, .T. ) ;
#7838=ORIENTED_EDGE ( 'NONE', *, *, #3943, .T. ) ;
#7862=EDGE_CURVE ( 'NONE', #10329, #3163, #4484, .T. ) ;
#7865=LINE ( 'NONE', #7631, #11851 ) ;
#7877=DIRECTION ( 'NONE',  ( 0.000000000000000000, 0.000000000000000000, -1.000000000000000000 ) ) ;
#7891=DIRECTION ( 'NONE',  ( 0.000000000000000000, 0.000000000000000000, -1.000000000000000000 ) ) ;
#7943=DIRECTION ( 'NONE',  ( 1.000000000000000000, 0.000000000000000000, 0.000000000000000000 ) ) ;
#7946=AXIS2_PLACEMENT_3D ( 'NONE', #7176, #5925, #1419 ) ;
#7959=CARTESIAN_POINT ( 'NONE',  ( 1.400000000000001910, 6.184466335694134054E-16, 5.000000000000000000 ) ) ;
#7968=EDGE_LOOP ( 'NONE', ( #13015, #13096, #3292, #12204 ) ) ;
#7997=( LENGTH_UNIT ( ) NAMED_UNIT ( * ) SI_UNIT ( .MILLI., .METRE. ) );
#8008=AXIS2_PLACEMENT_3D ( 'NONE', #5883, #11353, #8241 ) ;
#8055=EDGE_LOOP ( 'NONE', ( #11530, #8177 ) ) ;
#8077=FACE_OUTER_BOUND ( 'NONE', #1570, .T. ) ;
#8092=FACE_OUTER_BOUND ( 'NONE', #5082, .T. ) ;
#8153=VERTEX_POINT ( 'NONE', #10863 ) ;
#8173=ORIENTED_EDGE ( 'NONE', *, *, #10784, .F. ) ;
#8177=ORIENTED_EDGE ( 'NONE', *, *, #10784, .T. ) ;
#8180=AXIS2_PLACEMENT_3D ( 'NONE', #4132, #6261, #638 ) ;
#8208=DIRECTION ( 'NONE',  ( -0.000000000000000000, 0.000000000000000000, 1.000000000000000000 ) ) ;
#8220=TOROIDAL_SURFACE ( 'NONE', #8934, 7.399999999999999467, 0.1000000000000000472 ) ;
#8238=CIRCLE ( 'NONE', #11305, 0.1000000000000002554 ) ;
#8241=DIRECTION ( 'NONE',  ( 0.000000000000000000, -1.224646799147353454E-16, 1.000000000000000000 ) ) ;
#8243=ORIENTED_EDGE ( 'NONE', *, *, #11797, .T. ) ;
#8255=VERTEX_POINT ( 'NONE', #14107 ) ;
#8267=CARTESIAN_POINT ( 'NONE',  ( 1.500000000000001332, 0.000000000000000000, 0.000000000000000000 ) ) ;
#8296=ORIENTED_EDGE ( 'NONE', *, *, #10156, .T. ) ;
#8297=DIRECTION ( 'NONE',  ( 0.000000000000000000, 0.000000000000000000, -1.000000000000000000 ) ) ;
#8314=DIRECTION ( 'NONE',  ( 1.000000000000000000, 0.000000000000000000, 0.000000000000000000 ) ) ;
#8317=CARTESIAN_POINT ( 'NONE',  ( 1.500000000000001332, 0.000000000000000000, -7.399999999999999467 ) ) ;
#8331=ORIENTED_EDGE ( 'NONE', *, *, #12361, .F. ) ;
#8353=DIRECTION ( 'NONE',  ( 0.000000000000000000, 0.000000000000000000, -1.000000000000000000 ) ) ;
#8372=EDGE_CURVE ( 'NONE', #4002, #3163, #7078, .T. ) ;
#8379=CARTESIAN_POINT ( 'NONE',  ( 1.500000000000000888, 6.245698675651501825E-16, 5.100000000000000533 ) ) ;
#8389=EDGE_LOOP ( 'NONE', ( #14213, #2093 ) ) ;
#8397=( LENGTH_UNIT ( ) NAMED_UNIT ( * ) SI_UNIT ( .MILLI., .METRE. ) );
#8412=AXIS2_PLACEMENT_3D ( 'NONE', #5176, #4967, #6139 ) ;
#8426=DIRECTION ( 'NONE',  ( -1.000000000000000000, -0.000000000000000000, -0.000000000000000000 ) ) ;
#8427=DIRECTION ( 'NONE',  ( 1.000000000000000000, 0.000000000000000000, 0.000000000000000000 ) ) ;
#8487=CARTESIAN_POINT ( 'NONE',  ( 1.500000000000001332, 0.000000000000000000, 0.000000000000000000 ) ) ;
#8527=DIRECTION ( 'NONE',  ( 0.000000000000000000, 0.000000000000000000, -1.000000000000000000 ) ) ;
#8547=AXIS2_PLACEMENT_3D ( 'NONE', #8692, #7509, #9952 ) ;
#8553=VERTEX_POINT ( 'NONE', #11500 ) ;
#8554=PRODUCT ( 'angular contact ball bearing_68_iso_ISO 15 ABB - 1710 - 20,SI,NC,20_68', 'angular contact ball bearing_68_iso_ISO 15 ABB - 1710 - 20,SI,NC,20_68', '', ( #4513 ) ) ;
#8607=CARTESIAN_POINT ( 'NONE',  ( 1.400000000000001910, 0.000000000000000000, 0.000000000000000000 ) ) ;
#8631=DIRECTION ( 'NONE',  ( 0.000000000000000000, 0.000000000000000000, -1.000000000000000000 ) ) ;
#8634=ORIENTED_EDGE ( 'NONE', *, *, #11155, .F. ) ;
#8660=DIRECTION ( 'NONE',  ( -1.000000000000000000, -0.000000000000000000, -0.000000000000000000 ) ) ;
#8684=DIRECTION ( 'NONE',  ( 0.000000000000000000, 0.000000000000000000, -1.000000000000000000 ) ) ;
#8686=CIRCLE ( 'NONE', #6095, 7.500000000000000000 ) ;
#8692=CARTESIAN_POINT ( 'NONE',  ( 0.000000000000000000, 7.654042494670957606E-16, -6.250000000000000000 ) ) ;
#8699=ORIENTED_EDGE ( 'NONE', *, *, #13451, .F. ) ;
#8718=DIRECTION ( 'NONE',  ( 0.000000000000000000, 0.000000000000000000, -1.000000000000000000 ) ) ;
#8772=ORIENTED_EDGE ( 'NONE', *, *, #7350, .F. ) ;
#8774=DIRECTION ( 'NONE',  ( 0.000000000000000000, 0.000000000000000000, -1.000000000000000000 ) ) ;
#8782=CARTESIAN_POINT ( 'NONE',  ( 1.399999999999998579, 9.184850993605147944E-16, 7.500000000000000000 ) ) ;
#8846=DIRECTION ( 'NONE',  ( 0.000000000000000000, 0.000000000000000000, -1.000000000000000000 ) ) ;
#8847=FACE_OUTER_BOUND ( 'NONE', #5780, .T. ) ;
#8863=DIRECTION ( 'NONE',  ( 0.000000000000000000, 0.000000000000000000, -1.000000000000000000 ) ) ;
#8884=FACE_OUTER_BOUND ( 'NONE', #914, .T. ) ;
#8934=AXIS2_PLACEMENT_3D ( 'NONE', #10476, #1256, #5489 ) ;
#8948=AXIS2_PLACEMENT_3D ( 'NONE', #11340, #4483, #14520 ) ;
#8954=TOROIDAL_SURFACE ( 'NONE', #2594, 6.250000000000000000, 0.7500000000000000000 ) ;
#8960=DIRECTION ( 'NONE',  ( 0.000000000000000000, 0.000000000000000000, -1.000000000000000000 ) ) ;
#8971=ORIENTED_EDGE ( 'NONE', *, *, #4126, .F. ) ;
#8990=ORIENTED_EDGE ( 'NONE', *, *, #2401, .F. ) ;
#8997=CARTESIAN_POINT ( 'NONE',  ( -1.500000000000000888, 6.245698675651501825E-16, 5.100000000000000533 ) ) ;
#9018=AXIS2_PLACEMENT_3D ( 'NONE', #10666, #4369, #8863 ) ;
#9029=DIRECTION ( 'NONE',  ( 0.000000000000000000, 0.000000000000000000, -1.000000000000000000 ) ) ;
#9045=ORIENTED_EDGE ( 'NONE', *, *, #12054, .F. ) ;
#9058=CYLINDRICAL_SURFACE ( 'NONE', #4792, 5.000000000000000000 ) ;
#9066=DIRECTION ( 'NONE',  ( 0.000000000000000000, 0.000000000000000000, -1.000000000000000000 ) ) ;
#9081=DIRECTION ( 'NONE',  ( 1.000000000000000000, 0.000000000000000000, 0.000000000000000000 ) ) ;
#9154=CIRCLE ( 'NONE', #9865, 5.000000000000000000 ) ;
#9182=CARTESIAN_POINT ( 'NONE',  ( -1.399999999999998579, 0.000000000000000000, -7.500000000000000000 ) ) ;
#9214=DIRECTION ( 'NONE',  ( 1.000000000000000000, 0.000000000000000000, 0.000000000000000000 ) ) ;
#9251=FACE_OUTER_BOUND ( 'NONE', #505, .T. ) ;
#9260=ADVANCED_FACE ( 'NONE', ( #9251 ), #4678, .T. ) ;
#9266=ORIENTED_EDGE ( 'NONE', *, *, #222, .T. ) ;
#9270=VECTOR ( 'NONE', #6897, 1000.000000000000000 ) ;
#9308=DIRECTION ( 'NONE',  ( 0.000000000000000000, -1.000000000000000000, 0.000000000000000000 ) ) ;
#9325=ORIENTED_EDGE ( 'NONE', *, *, #9885, .F. ) ;
#9357=CYLINDRICAL_SURFACE ( 'NONE', #11772, 6.750000000000000000 ) ;
#9362=AXIS2_PLACEMENT_3D ( 'NONE', #4031, #7420, #8527 ) ;
#9370=ORIENTED_EDGE ( 'NONE', *, *, #8372, .F. ) ;
#9383=AXIS2_PLACEMENT_3D ( 'NONE', #3039, #12032, #7759 ) ;
#9396=AXIS2_PLACEMENT_3D ( 'NONE', #9468, #1411, #11593 ) ;
#9399=DIRECTION ( 'NONE',  ( 1.000000000000000000, 0.000000000000000000, 0.000000000000000000 ) ) ;
#9417=AXIS2_PLACEMENT_3D ( 'NONE', #1231, #2188, #3605 ) ;
#9424=ORIENTED_EDGE ( 'NONE', *, *, #10156, .F. ) ;
#9426=DIRECTION ( 'NONE',  ( 1.000000000000000000, 0.000000000000000000, 0.000000000000000000 ) ) ;
#9439=AXIS2_PLACEMENT_3D ( 'NONE', #9781, #6601, #11100 ) ;
#9440=AXIS2_PLACEMENT_3D ( 'NONE', #4347, #14302, #6417 ) ;
#9463=ORIENTED_EDGE ( 'NONE', *, *, #5983, .F. ) ;
#9468=CARTESIAN_POINT ( 'NONE',  ( 1.399999999999999689, 0.000000000000000000, -7.399999999999999467 ) ) ;
#9503=DIRECTION ( 'NONE',  ( 0.000000000000000000, 0.000000000000000000, -1.000000000000000000 ) ) ;
#9516=CLOSED_SHELL ( 'NONE', ( #13455, #7832, #6922, #5013, #9739, #14236, #11333, #11945, #10177, #9260, #3962, #7785, #13065, #2528, #7529, #6548, #4290, #5225, #7384, #13502, #6045, #4157, #11978, #7650, #4084, #11230, #1235, #14233 ) ) ;
#9551=EDGE_CURVE ( 'NONE', #5571, #11290, #11550, .T. ) ;
#9596=DIRECTION ( 'NONE',  ( 0.000000000000000000, 0.000000000000000000, -1.000000000000000000 ) ) ;
#9625=ORIENTED_EDGE ( 'NONE', *, *, #2560, .T. ) ;
#9644=( LENGTH_UNIT ( ) NAMED_UNIT ( * ) SI_UNIT ( .MILLI., .METRE. ) );
#9653=CARTESIAN_POINT ( 'NONE',  ( -20.63749999999999929, 0.000000000000000000, -5.750000000000000000 ) ) ;
#9667=TOROIDAL_SURFACE ( 'NONE', #6121, 7.399999999999999467, 0.1000000000000000472 ) ;
#9677=CARTESIAN_POINT ( 'NONE',  ( -1.500000000000001332, 9.123618653647779187E-16, 7.399999999999999467 ) ) ;
#9739=ADVANCED_FACE ( 'NONE', ( #6721 ), #14479, .F. ) ;
#9751=CARTESIAN_POINT ( 'NONE',  ( 1.500000000000001332, 0.000000000000000000, 0.000000000000000000 ) ) ;
#9764=CARTESIAN_POINT ( 'NONE',  ( 1.400000000000000133, 6.245698675651501825E-16, 5.100000000000000533 ) ) ;
#9781=CARTESIAN_POINT ( 'NONE',  ( -1.400000000000001910, 0.000000000000000000, 0.000000000000000000 ) ) ;
#9792=ORIENTED_EDGE ( 'NONE', *, *, #6281, .T. ) ;
#9794=ORIENTED_EDGE ( 'NONE', *, *, #1835, .F. ) ;
#9842=EDGE_LOOP ( 'NONE', ( #4151, #1982, #9266, #2051 ) ) ;
#9859=EDGE_LOOP ( 'NONE', ( #16, #5492, #7296, #1509 ) ) ;
#9865=AXIS2_PLACEMENT_3D ( 'NONE', #370, #305, #13911 ) ;
#9869=PLANE ( 'NONE',  #11759 ) ;
#9875=CIRCLE ( 'NONE', #12694, 6.750000000000000000 ) ;
#9879=DIRECTION ( 'NONE',  ( 1.000000000000000000, 0.000000000000000000, 0.000000000000000000 ) ) ;
#9884=CIRCLE ( 'NONE', #2332, 0.7499999999999997780 ) ;
#9885=EDGE_CURVE ( 'NONE', #2876, #3186, #721, .T. ) ;
#9886=AXIS2_PLACEMENT_3D ( 'NONE', #3225, #2941, #8774 ) ;
#9911=TOROIDAL_SURFACE ( 'NONE', #3078, 6.250000000000000000, 0.7500000000000000000 ) ;
#9917=DIRECTION ( 'NONE',  ( 0.000000000000000000, -1.000000000000000000, 0.000000000000000000 ) ) ;
#9951=FACE_OUTER_BOUND ( 'NONE', #3347, .T. ) ;
#9952=DIRECTION ( 'NONE',  ( 0.000000000000000000, -1.224646799147353454E-16, 1.000000000000000000 ) ) ;
#9954=ORIENTED_EDGE ( 'NONE', *, *, #11146, .F. ) ;
#9960=CARTESIAN_POINT ( 'NONE',  ( 1.399999999999998579, 0.000000000000000000, 0.000000000000000000 ) ) ;
#10011=DIRECTION ( 'NONE',  ( 1.000000000000000000, 0.000000000000000000, 0.000000000000000000 ) ) ;
#10022=DIRECTION ( 'NONE',  ( 1.000000000000000000, 0.000000000000000000, 0.000000000000000000 ) ) ;
#10087=DIRECTION ( 'NONE',  ( 0.000000000000000000, 0.000000000000000000, -1.000000000000000000 ) ) ;
#10116=CIRCLE ( 'NONE', #3055, 7.500000000000000000 ) ;
#10134=AXIS2_PLACEMENT_3D ( 'NONE', #3661, #4993, #8297 ) ;
#10139=ORIENTED_EDGE ( 'NONE', *, *, #10175, .F. ) ;
#10156=EDGE_CURVE ( 'NONE', #12082, #6460, #10870, .T. ) ;
#10175=EDGE_CURVE ( 'NONE', #4296, #3186, #2846, .T. ) ;
#10177=ADVANCED_FACE ( 'NONE', ( #648 ), #11093, .T. ) ;
#10178=COLOUR_RGB ( '',1.000000000000000000, 0.9490196078431372140, 0.9098039215686274384 ) ;
#10179=DIRECTION ( 'NONE',  ( 0.000000000000000000, 0.000000000000000000, -1.000000000000000000 ) ) ;
#10225=ORIENTED_EDGE ( 'NONE', *, *, #2228, .T. ) ;
#10259=DIRECTION ( 'NONE',  ( 0.000000000000000000, 0.000000000000000000, -1.000000000000000000 ) ) ;
#10269=EDGE_CURVE ( 'NONE', #1030, #13812, #12264, .T. ) ;
#10308=ORIENTED_EDGE ( 'NONE', *, *, #4852, .F. ) ;
#10325=EDGE_CURVE ( 'NONE', #8153, #2291, #6623, .T. ) ;
#10329=VERTEX_POINT ( 'NONE', #4287 ) ;
#10335=CIRCLE ( 'NONE', #7026, 7.500000000000000000 ) ;
#10357=DIRECTION ( 'NONE',  ( 1.000000000000000000, 0.000000000000000000, 0.000000000000000000 ) ) ;
#10413=EDGE_LOOP ( 'NONE', ( #8296, #12515, #1624, #8634 ) ) ;
#10467=FACE_OUTER_BOUND ( 'NONE', #9842, .T. ) ;
#10476=CARTESIAN_POINT ( 'NONE',  ( -1.399999999999999689, 0.000000000000000000, 0.000000000000000000 ) ) ;
#10484=CARTESIAN_POINT ( 'NONE',  ( 1.400000000000000133, 0.000000000000000000, 0.000000000000000000 ) ) ;
#10528=LINE ( 'NONE', #12446, #14154 ) ;
#10597=CARTESIAN_POINT ( 'NONE',  ( 1.500000000000001332, 0.000000000000000000, -6.750000000000000000 ) ) ;
#10601=ORIENTED_EDGE ( 'NONE', *, *, #4134, .F. ) ;
#10666=CARTESIAN_POINT ( 'NONE',  ( -20.63749999999999574, 0.000000000000000000, 0.000000000000000000 ) ) ;
#10671=AXIS2_PLACEMENT_3D ( 'NONE', #1350, #10357, #227 ) ;
#10754=CARTESIAN_POINT ( 'NONE',  ( 1.399999999999999689, 0.000000000000000000, 0.000000000000000000 ) ) ;
#10784=EDGE_CURVE ( 'NONE', #3186, #4296, #3103, .T. ) ;
#10816=VECTOR ( 'NONE', #3969, 1000.000000000000000 ) ;
#10860=CARTESIAN_POINT ( 'NONE',  ( 1.500000000000001332, 6.766173565289127388E-16, 5.525000000000000355 ) ) ;
#10863=CARTESIAN_POINT ( 'NONE',  ( -0.1920286436967154065, 0.000000000000000000, 6.975000000000000533 ) ) ;
#10868=DIRECTION ( 'NONE',  ( 1.000000000000000000, 0.000000000000000000, 0.000000000000000000 ) ) ;
#10870=CIRCLE ( 'NONE', #3323, 5.525000000000000355 ) ;
#10883=AXIS2_PLACEMENT_3D ( 'NONE', #2380, #14560, #9029 ) ;
#10884=CARTESIAN_POINT ( 'NONE',  ( -20.63749999999999574, 0.000000000000000000, 0.000000000000000000 ) ) ;
#10888=( GEOMETRIC_REPRESENTATION_CONTEXT ( 3 ) GLOBAL_UNCERTAINTY_ASSIGNED_CONTEXT ( ( #732 ) ) GLOBAL_UNIT_ASSIGNED_CONTEXT ( ( #9644, #2173, #4465 ) ) REPRESENTATION_CONTEXT ( 'NONE', 'WORKASPACE' ) );
#10911=AXIS2_PLACEMENT_3D ( 'NONE', #6022, #389, #6099 ) ;
#10919=ORIENTED_EDGE ( 'NONE', *, *, #4409, .F. ) ;
#10956=ORIENTED_EDGE ( 'NONE', *, *, #4501, .T. ) ;
#10973=EDGE_CURVE ( 'NONE', #8255, #689, #2874, .T. ) ;
#10999=CARTESIAN_POINT ( 'NONE',  ( -1.399999999999998579, 0.000000000000000000, 0.000000000000000000 ) ) ;
#11031=CIRCLE ( 'NONE', #6560, 5.525000000000000355 ) ;
#11050=CIRCLE ( 'NONE', #4705, 6.750000000000000000 ) ;
#11064=EDGE_LOOP ( 'NONE', ( #6902, #8243, #2916, #253 ) ) ;
#11089=LINE ( 'NONE', #4798, #7752 ) ;
#11093=TOROIDAL_SURFACE ( 'NONE', #4748, 5.100000000000000533, 0.1000000000000001582 ) ;
#11096=CARTESIAN_POINT ( 'NONE',  ( 1.500000000000001332, 9.123618653647779187E-16, 7.399999999999999467 ) ) ;
#11100=DIRECTION ( 'NONE',  ( 0.000000000000000000, 0.000000000000000000, -1.000000000000000000 ) ) ;
#11104=CARTESIAN_POINT ( 'NONE',  ( 1.399999999999999689, 0.000000000000000000, 0.000000000000000000 ) ) ;
#11146=EDGE_CURVE ( 'NONE', #6536, #5286, #690, .T. ) ;
#11155=EDGE_CURVE ( 'NONE', #12082, #8553, #1222, .T. ) ;
#11223=ORIENTED_EDGE ( 'NONE', *, *, #407, .T. ) ;
#11230=ADVANCED_FACE ( 'NONE', ( #6742 ), #14192, .T. ) ;
#11258=DIRECTION ( 'NONE',  ( 1.000000000000000000, 0.000000000000000000, 0.000000000000000000 ) ) ;
#11290=VERTEX_POINT ( 'NONE', #453 ) ;
#11295=DIRECTION ( 'NONE',  ( 0.000000000000000000, 0.000000000000000000, -1.000000000000000000 ) ) ;
#11305=AXIS2_PLACEMENT_3D ( 'NONE', #5563, #6813, #13385 ) ;
#11306=ORIENTED_EDGE ( 'NONE', *, *, #2854, .T. ) ;
#11315=CIRCLE ( 'NONE', #14389, 5.000000000000000000 ) ;
#11333=ADVANCED_FACE ( 'NONE', ( #4984 ), #2163, .T. ) ;
#11340=CARTESIAN_POINT ( 'NONE',  ( 0.5590169943749477843, 0.000000000000000000, 0.000000000000000000 ) ) ;
#11353=DIRECTION ( 'NONE',  ( -0.000000000000000000, 1.000000000000000000, 1.224646799147353207E-16 ) ) ;
#11384=EDGE_LOOP ( 'NONE', ( #9792, #13579, #5759, #6039 ) ) ;
#11500=CARTESIAN_POINT ( 'NONE',  ( 0.5590169943749478954, 0.000000000000000000, 6.750000000000000000 ) ) ;
#11524=AXIS2_PLACEMENT_3D ( 'NONE', #1159, #39, #10179 ) ;
#11530=ORIENTED_EDGE ( 'NONE', *, *, #10175, .T. ) ;
#11537=DIRECTION ( 'NONE',  ( 1.000000000000000000, 0.000000000000000000, 0.000000000000000000 ) ) ;
#11545=AXIS2_PLACEMENT_3D ( 'NONE', #4354, #9879, #5672 ) ;
#11550=CIRCLE ( 'NONE', #5900, 5.750000000000000000 ) ;
#11551=ORIENTED_EDGE ( 'NONE', *, *, #12627, .F. ) ;
#11556=DIRECTION ( 'NONE',  ( -1.000000000000000000, -0.000000000000000000, -0.000000000000000000 ) ) ;
#11559=LINE ( 'NONE', #7210, #200 ) ;
#11586=APPLICATION_CONTEXT ( 'automotive_design' ) ;
#11593=DIRECTION ( 'NONE',  ( 0.000000000000000000, 0.000000000000000000, -1.000000000000000000 ) ) ;
#11613=CARTESIAN_POINT ( 'NONE',  ( -20.63749999999999929, 7.041719095097280880E-16, 5.750000000000000000 ) ) ;
#11700=FACE_OUTER_BOUND ( 'NONE', #12272, .T. ) ;
#11705=CIRCLE ( 'NONE', #9362, 6.975000000000000533 ) ;
#11719=DIRECTION ( 'NONE',  ( 0.000000000000000000, -1.000000000000000000, 0.000000000000000000 ) ) ;
#11724=AXIS2_PLACEMENT_3D ( 'NONE', #3939, #8427, #7186 ) ;
#11745=LINE ( 'NONE', #11613, #12091 ) ;
#11759=AXIS2_PLACEMENT_3D ( 'NONE', #6415, #14456, #630 ) ;
#11772=AXIS2_PLACEMENT_3D ( 'NONE', #330, #402, #9066 ) ;
#11776=ADVANCED_BREP_SHAPE_REPRESENTATION ( '', ( #2170, #9440 ), #10888 ) ;
#11793=ORIENTED_EDGE ( 'NONE', *, *, #31, .T. ) ;
#11797=EDGE_CURVE ( 'NONE', #2291, #11290, #6666, .T. ) ;
#11810=STYLED_ITEM ( 'NONE', ( #1058 ), #11776 ) ;
#11851=VECTOR ( 'NONE', #13363, 1000.000000000000000 ) ;
#11870=EDGE_LOOP ( 'NONE', ( #1698, #11793, #1291, #7793 ) ) ;
#11900=CARTESIAN_POINT ( 'NONE',  ( 0.000000000000000000, 0.000000000000000000, 0.000000000000000000 ) ) ;
#11916=ORIENTED_EDGE ( 'NONE', *, *, #14089, .F. ) ;
#11945=ADVANCED_FACE ( 'NONE', ( #8092 ), #9058, .F. ) ;
#11946=CIRCLE ( 'NONE', #8180, 5.750000000000000000 ) ;
#11978=ADVANCED_FACE ( 'NONE', ( #14010 ), #5141, .F. ) ;
#11983=DIRECTION ( 'NONE',  ( 0.000000000000000000, 0.000000000000000000, -1.000000000000000000 ) ) ;
#12018=AXIS2_PLACEMENT_3D ( 'NONE', #3724, #2688, #8208 ) ;
#12032=DIRECTION ( 'NONE',  ( 1.000000000000000000, 0.000000000000000000, 0.000000000000000000 ) ) ;
#12054=EDGE_CURVE ( 'NONE', #6460, #12082, #1712, .T. ) ;
#12082=VERTEX_POINT ( 'NONE', #5508 ) ;
#12084=FACE_OUTER_BOUND ( 'NONE', #5822, .T. ) ;
#12091=VECTOR ( 'NONE', #11537, 1000.000000000000000 ) ;
#12153=VERTEX_POINT ( 'NONE', #14288 ) ;
#12165=CARTESIAN_POINT ( 'NONE',  ( 0.000000000000000000, 0.000000000000000000, 0.000000000000000000 ) ) ;
#12170=ORIENTED_EDGE ( 'NONE', *, *, #3737, .T. ) ;
#12204=ORIENTED_EDGE ( 'NONE', *, *, #222, .F. ) ;
#12206=CARTESIAN_POINT ( 'NONE',  ( 0.5590169943749478954, 8.266365894244635319E-16, -6.750000000000000000 ) ) ;
#12242=CARTESIAN_POINT ( 'NONE',  ( -1.500000000000001332, 0.000000000000000000, 0.000000000000000000 ) ) ;
#12243=ORIENTED_EDGE ( 'NONE', *, *, #2228, .F. ) ;
#12248=EDGE_CURVE ( 'NONE', #4518, #796, #1127, .T. ) ;
#12264=CIRCLE ( 'NONE', #1664, 6.750000000000000000 ) ;
#12272=EDGE_LOOP ( 'NONE', ( #8990, #10956, #12633, #2409 ) ) ;
#12279=SURFACE_STYLE_USAGE ( .BOTH. , #4394 ) ;
#12287=VECTOR ( 'NONE', #6468, 1000.000000000000000 ) ;
#12327=EDGE_CURVE ( 'NONE', #3448, #5571, #11745, .T. ) ;
#12353=( NAMED_UNIT ( * ) PLANE_ANGLE_UNIT ( ) SI_UNIT ( $, .RADIAN. ) );
#12361=EDGE_CURVE ( 'NONE', #10329, #4518, #9154, .T. ) ;
#12376=DIRECTION ( 'NONE',  ( 0.000000000000000000, 0.000000000000000000, -1.000000000000000000 ) ) ;
#12409=CARTESIAN_POINT ( 'NONE',  ( -20.63749999999999574, 0.000000000000000000, 0.000000000000000000 ) ) ;
#12423=ORIENTED_EDGE ( 'NONE', *, *, #2742, .T. ) ;
#12446=CARTESIAN_POINT ( 'NONE',  ( -20.63749999999999929, 0.000000000000000000, -5.525000000000000355 ) ) ;
#12492=CARTESIAN_POINT ( 'NONE',  ( -1.500000000000001332, 0.000000000000000000, 0.000000000000000000 ) ) ;
#12515=ORIENTED_EDGE ( 'NONE', *, *, #4126, .T. ) ;
#12549=ORIENTED_EDGE ( 'NONE', *, *, #13630, .T. ) ;
#12553=EDGE_CURVE ( 'NONE', #5458, #2876, #14421, .T. ) ;
#12568=ORIENTED_EDGE ( 'NONE', *, *, #12054, .T. ) ;
#12627=EDGE_CURVE ( 'NONE', #12082, #12943, #11089, .T. ) ;
#12633=ORIENTED_EDGE ( 'NONE', *, *, #3856, .T. ) ;
#12689=ORIENTED_EDGE ( 'NONE', *, *, #9885, .T. ) ;
#12694=AXIS2_PLACEMENT_3D ( 'NONE', #7705, #5557, #13311 ) ;
#12713=CARTESIAN_POINT ( 'NONE',  ( 1.500000000000001332, 0.000000000000000000, 0.000000000000000000 ) ) ;
#12718=FACE_OUTER_BOUND ( 'NONE', #11064, .T. ) ;
#12735=CARTESIAN_POINT ( 'NONE',  ( -0.1920286436967154065, 8.541911424052788811E-16, -6.975000000000000533 ) ) ;
#12751=AXIS2_PLACEMENT_3D ( 'NONE', #3191, #2216, #7628 ) ;
#12783=EDGE_CURVE ( 'NONE', #5286, #4296, #7504, .T. ) ;
#12848=DIRECTION ( 'NONE',  ( 0.000000000000000000, 0.000000000000000000, -1.000000000000000000 ) ) ;
#12933=VECTOR ( 'NONE', #5702, 1000.000000000000000 ) ;
#12943=VERTEX_POINT ( 'NONE', #10860 ) ;
#12965=AXIS2_PLACEMENT_3D ( 'NONE', #10884, #760, #3056 ) ;
#12967=VERTEX_POINT ( 'NONE', #14321 ) ;
#13011=CARTESIAN_POINT ( 'NONE',  ( -0.5590169943749470072, 0.000000000000000000, 0.000000000000000000 ) ) ;
#13015=ORIENTED_EDGE ( 'NONE', *, *, #3188, .F. ) ;
#13048=CARTESIAN_POINT ( 'NONE',  ( -1.400000000000000133, 0.000000000000000000, 0.000000000000000000 ) ) ;
#13065=ADVANCED_FACE ( 'NONE', ( #7834 ), #13884, .T. ) ;
#13087=ORIENTED_EDGE ( 'NONE', *, *, #2590, .F. ) ;
#13096=ORIENTED_EDGE ( 'NONE', *, *, #4848, .T. ) ;
#13099=ORIENTED_EDGE ( 'NONE', *, *, #13249, .T. ) ;
#13111=DIRECTION ( 'NONE',  ( 1.000000000000000000, 0.000000000000000000, 0.000000000000000000 ) ) ;
#13132=CARTESIAN_POINT ( 'NONE',  ( 1.500000000000000888, 0.000000000000000000, -5.100000000000000533 ) ) ;
#13148=FACE_OUTER_BOUND ( 'NONE', #14572, .T. ) ;
#13177=AXIS2_PLACEMENT_3D ( 'NONE', #12165, #13288, #7683 ) ;
#13189=DIRECTION ( 'NONE',  ( 1.000000000000000000, 0.000000000000000000, 0.000000000000000000 ) ) ;
#13249=EDGE_CURVE ( 'NONE', #796, #12967, #13646, .T. ) ;
#13257=AXIS2_PLACEMENT_3D ( 'NONE', #5416, #9917, #14424 ) ;
#13278=ORIENTED_EDGE ( 'NONE', *, *, #2590, .T. ) ;
#13283=CARTESIAN_POINT ( 'NONE',  ( 1.399999999999998579, 0.000000000000000000, -7.500000000000000000 ) ) ;
#13284=DIRECTION ( 'NONE',  ( 1.000000000000000000, 0.000000000000000000, 0.000000000000000000 ) ) ;
#13288=DIRECTION ( 'NONE',  ( -1.000000000000000000, -0.000000000000000000, -0.000000000000000000 ) ) ;
#13309=ORIENTED_EDGE ( 'NONE', *, *, #12783, .F. ) ;
#13311=DIRECTION ( 'NONE',  ( 0.000000000000000000, 0.000000000000000000, 1.000000000000000000 ) ) ;
#13336=EDGE_CURVE ( 'NONE', #4733, #12153, #7776, .T. ) ;
#13345=DIRECTION ( 'NONE',  ( 1.000000000000000000, 0.000000000000000000, 0.000000000000000000 ) ) ;
#13363=DIRECTION ( 'NONE',  ( 1.000000000000000000, 0.000000000000000000, 0.000000000000000000 ) ) ;
#13365=STYLED_ITEM('',(#14674),#2170);
#13366=TOROIDAL_SURFACE ( 'NONE', #7946, 6.250000000000000000, 0.7500000000000000000 ) ;
#13385=DIRECTION ( 'NONE',  ( 0.000000000000000000, 1.224646799147343593E-16, 1.000000000000000000 ) ) ;
#13425=CIRCLE ( 'NONE', #8948, 6.750000000000000000 ) ;
#13451=EDGE_CURVE ( 'NONE', #11290, #5571, #4007, .T. ) ;
#13455=ADVANCED_FACE ( 'NONE', ( #12084 ), #9667, .T. ) ;
#13482=AXIS2_PLACEMENT_3D ( 'NONE', #1739, #7202, #5956 ) ;
#13487=ORIENTED_EDGE ( 'NONE', *, *, #3943, .F. ) ;
#13502=ADVANCED_FACE ( 'NONE', ( #6256, #9951 ), #9869, .T. ) ;
#13539=ORIENTED_EDGE ( 'NONE', *, *, #12553, .T. ) ;
#13579=ORIENTED_EDGE ( 'NONE', *, *, #2401, .T. ) ;
#13598=EDGE_CURVE ( 'NONE', #5688, #8553, #13425, .T. ) ;
#13608=DIRECTION ( 'NONE',  ( 1.000000000000000000, 0.000000000000000000, 0.000000000000000000 ) ) ;
#13610=SURFACE_STYLE_FILL_AREA ( #4620 ) ;
#13630=EDGE_CURVE ( 'NONE', #12153, #4733, #14601, .T. ) ;
#13646=CIRCLE ( 'NONE', #189, 5.000000000000000000 ) ;
#13653=ORIENTED_EDGE ( 'NONE', *, *, #12627, .T. ) ;
#13660=APPLICATION_CONTEXT ( 'automotive_design' ) ;
#13679=DIRECTION ( 'NONE',  ( 0.000000000000000000, 0.000000000000000000, -1.000000000000000000 ) ) ;
#13688=FACE_BOUND ( 'NONE', #6524, .T. ) ;
#13731=ORIENTED_EDGE ( 'NONE', *, *, #9551, .T. ) ;
#13753=ORIENTED_EDGE ( 'NONE', *, *, #25, .T. ) ;
#13801=( NAMED_UNIT ( * ) PLANE_ANGLE_UNIT ( ) SI_UNIT ( $, .RADIAN. ) );
#13809=DIRECTION ( 'NONE',  ( 0.000000000000000000, 0.000000000000000000, -1.000000000000000000 ) ) ;
#13812=VERTEX_POINT ( 'NONE', #10597 ) ;
#13826=PLANE ( 'NONE',  #12018 ) ;
#13831=VERTEX_POINT ( 'NONE', #8379 ) ;
#13882=DIRECTION ( 'NONE',  ( -1.000000000000000000, -0.000000000000000000, -0.000000000000000000 ) ) ;
#13884=TOROIDAL_SURFACE ( 'NONE', #13177, 6.250000000000000000, 0.7500000000000000000 ) ;
#13903=DIRECTION ( 'NONE',  ( 0.000000000000000000, 1.000000000000000000, -1.224646799147353207E-16 ) ) ;
#13911=DIRECTION ( 'NONE',  ( 0.000000000000000000, 0.000000000000000000, -1.000000000000000000 ) ) ;
#13954=( NAMED_UNIT ( * ) SI_UNIT ( $, .STERADIAN. ) SOLID_ANGLE_UNIT ( ) );
#13986=EDGE_LOOP ( 'NONE', ( #5881, #13539, #6405, #9954 ) ) ;
#14010=FACE_OUTER_BOUND ( 'NONE', #9859, .T. ) ;
#14089=EDGE_CURVE ( 'NONE', #689, #5458, #8238, .T. ) ;
#14099=DIRECTION ( 'NONE',  ( 1.000000000000000000, 0.000000000000000000, 0.000000000000000000 ) ) ;
#14107=CARTESIAN_POINT ( 'NONE',  ( -1.500000000000001332, 0.000000000000000000, -7.399999999999999467 ) ) ;
#14154=VECTOR ( 'NONE', #9214, 1000.000000000000000 ) ;
#14192=TOROIDAL_SURFACE ( 'NONE', #5703, 7.399999999999999467, 0.1000000000000000472 ) ;
#14213=ORIENTED_EDGE ( 'NONE', *, *, #3376, .F. ) ;
#14233=ADVANCED_FACE ( 'NONE', ( #5938, #301 ), #13826, .T. ) ;
#14236=ADVANCED_FACE ( 'NONE', ( #12718 ), #9911, .T. ) ;
#14288=CARTESIAN_POINT ( 'NONE',  ( -1.500000000000001332, 8.541911424052788811E-16, 6.975000000000000533 ) ) ;
#14291=DIRECTION ( 'NONE',  ( 0.000000000000000000, 0.000000000000000000, -1.000000000000000000 ) ) ;
#14302=DIRECTION ( 'NONE',  ( 0.000000000000000000, 0.000000000000000000, 1.000000000000000000 ) ) ;
#14307=ORIENTED_EDGE ( 'NONE', *, *, #3066, .T. ) ;
#14321=CARTESIAN_POINT ( 'NONE',  ( 1.400000000000001910, 0.000000000000000000, -5.000000000000000000 ) ) ;
#14349=CIRCLE ( 'NONE', #8412, 0.1000000000000002554 ) ;
#14389=AXIS2_PLACEMENT_3D ( 'NONE', #4849, #11258, #3665 ) ;
#14408=AXIS2_PLACEMENT_3D ( 'NONE', #2323, #1144, #3604 ) ;
#14416=MECHANICAL_DESIGN_GEOMETRIC_PRESENTATION_REPRESENTATION('',(#11810),#1684);
#14421=LINE ( 'NONE', #4313, #12933 ) ;
#14424=DIRECTION ( 'NONE',  ( 0.000000000000000000, 0.000000000000000000, -1.000000000000000000 ) ) ;
#14456=DIRECTION ( 'NONE',  ( -1.000000000000000000, 0.000000000000000000, -0.000000000000000000 ) ) ;
#14462=DIRECTION ( 'NONE',  ( 1.000000000000000000, 0.000000000000000000, 0.000000000000000000 ) ) ;
#14467=DIRECTION ( 'NONE',  ( -1.000000000000000000, -0.000000000000000000, -0.000000000000000000 ) ) ;
#14476=ORIENTED_EDGE ( 'NONE', *, *, #2803, .T. ) ;
#14479=CYLINDRICAL_SURFACE ( 'NONE', #9018, 6.750000000000000000 ) ;
#14505=SHAPE_REPRESENTATION_RELATIONSHIP ( 'NONE' , 'NONE' ,  #3781, #11776 ) ;
#14520=DIRECTION ( 'NONE',  ( 0.000000000000000000, 0.000000000000000000, 1.000000000000000000 ) ) ;
#14556=AXIS2_PLACEMENT_3D ( 'NONE', #8267, #7090, #516 ) ;
#14560=DIRECTION ( 'NONE',  ( 1.000000000000000000, 0.000000000000000000, 0.000000000000000000 ) ) ;
#14564=CARTESIAN_POINT ( 'NONE',  ( -20.63749999999999574, 8.266365894244634333E-16, 6.750000000000000000 ) ) ;
#14572=EDGE_LOOP ( 'NONE', ( #11551, #9045, #6649, #6903 ) ) ;
#14574=DIRECTION ( 'NONE',  ( 0.000000000000000000, 0.000000000000000000, -1.000000000000000000 ) ) ;
#14601=CIRCLE ( 'NONE', #9417, 6.975000000000000533 ) ;
#14604=CYLINDRICAL_SURFACE ( 'NONE', #11545, 7.500000000000000000 ) ;
#14668=COLOUR_RGB('Grey',0.48,0.52,0.57);
#14669=FILL_AREA_STYLE_COLOUR('',#14668);
#14670=FILL_AREA_STYLE('',(#14669));
#14671=SURFACE_STYLE_FILL_AREA(#14670);
#14672=SURFACE_SIDE_STYLE('',(#14671));
#14673=SURFACE_STYLE_USAGE(.BOTH.,#14672);
#14674=PRESENTATION_STYLE_ASSIGNMENT((#14673));
ENDSEC;
END-ISO-10303-21;
